ISO-10303-21;
HEADER;
FILE_DESCRIPTION (('STEP AP214'),
    '1' );
FILE_NAME ('double end studs bm=1.5d_am_AM A M8X100-N.step',
    '2026-10-08T05:56:58',
    ( '' ),
    ( '' ),
    'SwSTEP 2.0',
    'SolidWorks 2026',
    '' );
FILE_SCHEMA (( 'AUTOMOTIVE_DESIGN' ));
ENDSEC;

DATA;
#1=ORIENTED_EDGE ( 'NONE', *, *, #18394, .T. ) ;
#33=AXIS2_PLACEMENT_3D ( 'NONE', #19448, #5737, #11851 ) ;
#62=VERTEX_POINT ( 'NONE', #2132 ) ;
#97=AXIS2_PLACEMENT_3D ( 'NONE', #19744, #12155, #18353 ) ;
#131=AXIS2_PLACEMENT_3D ( 'NONE', #16442, #16336, #16243 ) ;
#176=ORIENTED_EDGE ( 'NONE', *, *, #9057, .T. ) ;
#192=AXIS2_PLACEMENT_3D ( 'NONE', #8954, #15156, #10755 ) ;
#217=CARTESIAN_POINT ( 'NONE',  ( -1.310841663519413114, 4.898587196589412829E-16, -4.000000000000000000 ) ) ;
#220=DIRECTION ( 'NONE',  ( 1.000000000000000000, 0.000000000000000000, 0.000000000000000000 ) ) ;
#259=EDGE_CURVE ( 'NONE', #12604, #8838, #10645, .T. ) ;
#285=EDGE_CURVE ( 'NONE', #19646, #4617, #17355, .T. ) ;
#335=ORIENTED_EDGE ( 'NONE', *, *, #16315, .T. ) ;
#394=DIRECTION ( 'NONE',  ( -1.000000000000000000, -0.000000000000000000, -0.000000000000000000 ) ) ;
#414=STYLED_ITEM ( 'NONE', ( #11361 ), #2965 ) ;
#449=VECTOR ( 'NONE', #17519, 1000.000000000000227 ) ;
#533=AXIS2_PLACEMENT_3D ( 'NONE', #9932, #13023, #14624 ) ;
#548=CIRCLE ( 'NONE', #12037, 4.000000000000000000 ) ;
#628=ORIENTED_EDGE ( 'NONE', *, *, #19583, .T. ) ;
#663=VECTOR ( 'NONE', #1603, 1000.000000000000000 ) ;
#667=EDGE_CURVE ( 'NONE', #62, #18274, #7812, .T. ) ;
#717=CONICAL_SURFACE ( 'NONE', #10300, 3.593999999999999861, 0.2132412839022293782 ) ;
#731=EDGE_CURVE ( 'NONE', #4617, #19646, #9712, .T. ) ;
#774=EDGE_CURVE ( 'NONE', #12919, #10924, #14811, .T. ) ;
#779=CONICAL_SURFACE ( 'NONE', #10686, 3.323500000000020993, 0.7853981633974463916 ) ;
#864=ORIENTED_EDGE ( 'NONE', *, *, #1510, .F. ) ;
#900=ADVANCED_FACE ( 'NONE', ( #16311 ), #10983, .T. ) ;
#965=CIRCLE ( 'NONE', #11818, 3.796999999999998820 ) ;
#1171=DIRECTION ( 'NONE',  ( -1.000000000000000000, -0.000000000000000000, -0.000000000000000000 ) ) ;
#1278=VERTEX_POINT ( 'NONE', #11394 ) ;
#1352=VECTOR ( 'NONE', #7469, 1000.000000000000114 ) ;
#1380=ADVANCED_FACE ( 'NONE', ( #10775 ), #779, .T. ) ;
#1460=ORIENTED_EDGE ( 'NONE', *, *, #9951, .F. ) ;
#1488=ORIENTED_EDGE ( 'NONE', *, *, #5537, .T. ) ;
#1503=( NAMED_UNIT ( * ) PLANE_ANGLE_UNIT ( ) SI_UNIT ( $, .RADIAN. ) );
#1510=EDGE_CURVE ( 'NONE', #2117, #62, #2040, .T. ) ;
#1522=VECTOR ( 'NONE', #13308, 1000.000000000000000 ) ;
#1567=PRODUCT_DEFINITION_FORMATION_WITH_SPECIFIED_SOURCE ( 'ANY', '', #13062, .NOT_KNOWN. ) ;
#1603=DIRECTION ( 'NONE',  ( 0.7071067811865489050, 8.659560562354915602E-17, 0.7071067811865462405 ) ) ;
#1658=DIRECTION ( 'NONE',  ( 0.9773501006361904331, 2.591706245282795403E-17, 0.2116288751244229938 ) ) ;
#1691=ORIENTED_EDGE ( 'NONE', *, *, #3954, .F. ) ;
#1763=VERTEX_POINT ( 'NONE', #9934 ) ;
#1838=EDGE_CURVE ( 'NONE', #8958, #17114, #10701, .T. ) ;
#1933=FACE_OUTER_BOUND ( 'NONE', #16792, .T. ) ;
#1963=ORIENTED_EDGE ( 'NONE', *, *, #19516, .F. ) ;
#1970=VECTOR ( 'NONE', #12424, 1000.000000000000000 ) ;
#1980=CONICAL_SURFACE ( 'NONE', #4223, 4.000000000000000000, 0.7853981633974458365 ) ;
#2022=AXIS2_PLACEMENT_3D ( 'NONE', #11853, #5645, #11957 ) ;
#2040=CIRCLE ( 'NONE', #131, 3.796999999999998820 ) ;
#2041=VERTEX_POINT ( 'NONE', #19607 ) ;
#2048=ORIENTED_EDGE ( 'NONE', *, *, #10407, .F. ) ;
#2117=VERTEX_POINT ( 'NONE', #8087 ) ;
#2132=CARTESIAN_POINT ( 'NONE',  ( 90.56249999999998579, 4.774285546475956322E-16, -3.796999999999998820 ) ) ;
#2206=EDGE_LOOP ( 'NONE', ( #19649, #8022, #10736, #4136 ) ) ;
#2259=DIRECTION ( 'NONE',  ( -1.000000000000000000, -0.000000000000000000, -0.000000000000000000 ) ) ;
#2280=APPLICATION_CONTEXT ( 'automotive_design' ) ;
#2305=CARTESIAN_POINT ( 'NONE',  ( 12.00000000000000000, 0.000000000000000000, 3.593999999999999861 ) ) ;
#2337=ADVANCED_FACE ( 'NONE', ( #5573 ), #1980, .T. ) ;
#2339=PRODUCT_DEFINITION ( 'UNKNOWN', '', #1567, #18196 ) ;
#2342=SURFACE_STYLE_FILL_AREA ( #17651 ) ;
#2383=EDGE_LOOP ( 'NONE', ( #11428, #15343, #7208, #3839 ) ) ;
#2406=CARTESIAN_POINT ( 'NONE',  ( 90.56249999999998579, 0.000000000000000000, 0.000000000000000000 ) ) ;
#2449=AXIS2_PLACEMENT_3D ( 'NONE', #4135, #16247, #10249 ) ;
#2510=EDGE_LOOP ( 'NONE', ( #7828, #1460, #3224, #15446 ) ) ;
#2587=DIRECTION ( 'NONE',  ( 1.000000000000000000, 0.000000000000000000, 0.000000000000000000 ) ) ;
#2655=DIRECTION ( 'NONE',  ( 0.000000000000000000, 0.000000000000000000, 1.000000000000000000 ) ) ;
#2722=CIRCLE ( 'NONE', #5285, 3.797000000000000597 ) ;
#2752=VECTOR ( 'NONE', #14520, 1000.000000000000000 ) ;
#2791=CARTESIAN_POINT ( 'NONE',  ( 0.000000000000000000, 0.000000000000000000, -3.323500000000020993 ) ) ;
#2807=CARTESIAN_POINT ( 'NONE',  ( -1.310841663519413114, 0.000000000000000000, 4.000000000000000000 ) ) ;
#2964=( GEOMETRIC_REPRESENTATION_CONTEXT ( 3 ) GLOBAL_UNCERTAINTY_ASSIGNED_CONTEXT ( ( #14797 ) ) GLOBAL_UNIT_ASSIGNED_CONTEXT ( ( #9869, #16161, #8249 ) ) REPRESENTATION_CONTEXT ( 'NONE', 'WORKASPACE' ) );
#2965=MANIFOLD_SOLID_BREP ( 'BaseBody', #15109 ) ;
#2996=ORIENTED_EDGE ( 'NONE', *, *, #13252, .F. ) ;
#3058=AXIS2_PLACEMENT_3D ( 'NONE', #16675, #18273, #13460 ) ;
#3159=CARTESIAN_POINT ( 'NONE',  ( -1.310841663519413114, 0.000000000000000000, 4.000000000000000000 ) ) ;
#3224=ORIENTED_EDGE ( 'NONE', *, *, #774, .T. ) ;
#3299=LINE ( 'NONE', #13706, #7681 ) ;
#3308=ORIENTED_EDGE ( 'NONE', *, *, #1838, .T. ) ;
#3355=EDGE_LOOP ( 'NONE', ( #8266, #15339 ) ) ;
#3421=EDGE_LOOP ( 'NONE', ( #16276, #13714, #628, #16669 ) ) ;
#3431=FACE_OUTER_BOUND ( 'NONE', #14729, .T. ) ;
#3443=CARTESIAN_POINT ( 'NONE',  ( 0.000000000000000000, 0.000000000000000000, 0.000000000000000000 ) ) ;
#3475=VECTOR ( 'NONE', #5538, 1000.000000000000114 ) ;
#3517=DIRECTION ( 'NONE',  ( 0.000000000000000000, 0.000000000000000000, 1.000000000000000000 ) ) ;
#3520=ORIENTED_EDGE ( 'NONE', *, *, #15902, .T. ) ;
#3764=FACE_OUTER_BOUND ( 'NONE', #3355, .T. ) ;
#3790=FACE_OUTER_BOUND ( 'NONE', #14284, .T. ) ;
#3792=UNCERTAINTY_MEASURE_WITH_UNIT (LENGTH_MEASURE( 1.000000000000000082E-05 ), #10030, 'distance_accuracy_value', 'NONE');
#3810=FACE_OUTER_BOUND ( 'NONE', #9635, .T. ) ;
#3811=DIRECTION ( 'NONE',  ( 0.000000000000000000, 0.000000000000000000, 1.000000000000000000 ) ) ;
#3839=ORIENTED_EDGE ( 'NONE', *, *, #1838, .F. ) ;
#3876=AXIS2_PLACEMENT_3D ( 'NONE', #17878, #1171, #4169 ) ;
#3942=SURFACE_STYLE_USAGE ( .BOTH. , #15859 ) ;
#3954=EDGE_CURVE ( 'NONE', #15369, #17299, #17816, .T. ) ;
#3989=DIRECTION ( 'NONE',  ( 0.000000000000000000, 0.000000000000000000, 1.000000000000000000 ) ) ;
#4010=( NAMED_UNIT ( * ) PLANE_ANGLE_UNIT ( ) SI_UNIT ( $, .RADIAN. ) );
#4072=CARTESIAN_POINT ( 'NONE',  ( 111.3234999999999957, 4.898587196589412829E-16, -4.000000000000000000 ) ) ;
#4135=CARTESIAN_POINT ( 'NONE',  ( 91.50000000000000000, 0.000000000000000000, 0.000000000000000000 ) ) ;
#4136=ORIENTED_EDGE ( 'NONE', *, *, #15282, .F. ) ;
#4169=DIRECTION ( 'NONE',  ( 0.000000000000000000, 0.000000000000000000, 1.000000000000000000 ) ) ;
#4172=CARTESIAN_POINT ( 'NONE',  ( 11.06250000000000000, 0.000000000000000000, 0.000000000000000000 ) ) ;
#4223=AXIS2_PLACEMENT_3D ( 'NONE', #12998, #8290, #16292 ) ;
#4264=STYLED_ITEM ( 'NONE', ( #8422 ), #8048 ) ;
#4268=DIRECTION ( 'NONE',  ( -1.000000000000000000, -0.000000000000000000, -0.000000000000000000 ) ) ;
#4271=AXIS2_PLACEMENT_3D ( 'NONE', #15429, #9430, #18714 ) ;
#4305=LINE ( 'NONE', #10321, #7030 ) ;
#4332=ORIENTED_EDGE ( 'NONE', *, *, #5772, .F. ) ;
#4338=DIRECTION ( 'NONE',  ( 0.000000000000000000, 0.000000000000000000, -1.000000000000000000 ) ) ;
#4425=ORIENTED_EDGE ( 'NONE', *, *, #6029, .F. ) ;
#4429=CYLINDRICAL_SURFACE ( 'NONE', #7246, 4.000000000000000000 ) ;
#4465=FACE_OUTER_BOUND ( 'NONE', #7126, .T. ) ;
#4482=ADVANCED_FACE ( 'NONE', ( #3431 ), #5223, .T. ) ;
#4564=LINE ( 'NONE', #3159, #10938 ) ;
#4582=CARTESIAN_POINT ( 'NONE',  ( 111.3234999999999957, 0.000000000000000000, 4.000000000000000000 ) ) ;
#4617=VERTEX_POINT ( 'NONE', #4710 ) ;
#4701=ORIENTED_EDGE ( 'NONE', *, *, #16315, .F. ) ;
#4710=CARTESIAN_POINT ( 'NONE',  ( 0.000000000000000000, 4.484350416777833449E-16, 3.323500000000020993 ) ) ;
#4904=DIRECTION ( 'NONE',  ( -1.000000000000000000, -0.000000000000000000, -0.000000000000000000 ) ) ;
#4928=ORIENTED_EDGE ( 'NONE', *, *, #731, .F. ) ;
#4980=ORIENTED_EDGE ( 'NONE', *, *, #15753, .F. ) ;
#5024=EDGE_CURVE ( 'NONE', #18274, #19129, #17517, .T. ) ;
#5045=PRODUCT_CONTEXT ( 'NONE', #16226, 'mechanical' ) ;
#5075=ORIENTED_EDGE ( 'NONE', *, *, #11034, .T. ) ;
#5110=DIRECTION ( 'NONE',  ( -1.000000000000000000, -0.000000000000000000, -0.000000000000000000 ) ) ;
#5151=CONICAL_SURFACE ( 'NONE', #3876, 4.000000000000000000, 0.7853981633974458365 ) ;
#5205=AXIS2_PLACEMENT_3D ( 'NONE', #16859, #6133, #5935 ) ;
#5223=CYLINDRICAL_SURFACE ( 'NONE', #8250, 4.000000000000000000 ) ;
#5231=ADVANCED_FACE ( 'NONE', ( #4465 ), #14775, .T. ) ;
#5259=DIRECTION ( 'NONE',  ( -0.000000000000000000, 0.000000000000000000, 1.000000000000000000 ) ) ;
#5280=EDGE_CURVE ( 'NONE', #17299, #15369, #12004, .T. ) ;
#5285=AXIS2_PLACEMENT_3D ( 'NONE', #12059, #15554, #18646 ) ;
#5346=CONICAL_SURFACE ( 'NONE', #2449, 3.593999999999999861, 0.2132412839022289897 ) ;
#5445=CIRCLE ( 'NONE', #16629, 4.000000000000000000 ) ;
#5466=ORIENTED_EDGE ( 'NONE', *, *, #10417, .F. ) ;
#5490=LINE ( 'NONE', #13206, #2752 ) ;
#5537=EDGE_CURVE ( 'NONE', #17114, #8958, #12342, .T. ) ;
#5538=DIRECTION ( 'NONE',  ( -0.7071067811865492381, 8.659560562354910671E-17, -0.7071067811865457964 ) ) ;
#5573=FACE_OUTER_BOUND ( 'NONE', #16038, .T. ) ;
#5591=DIRECTION ( 'NONE',  ( 0.000000000000000000, 0.000000000000000000, -1.000000000000000000 ) ) ;
#5641=ORIENTED_EDGE ( 'NONE', *, *, #16786, .F. ) ;
#5645=DIRECTION ( 'NONE',  ( -1.000000000000000000, -0.000000000000000000, -0.000000000000000000 ) ) ;
#5682=CARTESIAN_POINT ( 'NONE',  ( 10.12500000000000178, 4.898587196589412829E-16, -4.000000000000000000 ) ) ;
#5718=CARTESIAN_POINT ( 'NONE',  ( 12.00000000000000355, 0.000000000000000000, 0.000000000000000000 ) ) ;
#5725=LINE ( 'NONE', #10063, #3475 ) ;
#5729=CARTESIAN_POINT ( 'NONE',  ( 12.00000000000000355, 4.898587196589412829E-16, 4.000000000000000000 ) ) ;
#5737=DIRECTION ( 'NONE',  ( 1.000000000000000000, 0.000000000000000000, 0.000000000000000000 ) ) ;
#5772=EDGE_CURVE ( 'NONE', #19129, #9230, #9019, .T. ) ;
#5903=DIRECTION ( 'NONE',  ( 0.000000000000000000, 0.000000000000000000, 1.000000000000000000 ) ) ;
#5910=VECTOR ( 'NONE', #17937, 999.9999999999998863 ) ;
#5924=DIRECTION ( 'NONE',  ( 1.000000000000000000, 0.000000000000000000, 0.000000000000000000 ) ) ;
#5925=CARTESIAN_POINT ( 'NONE',  ( -1.310841663519413114, 0.000000000000000000, 0.000000000000000000 ) ) ;
#5935=DIRECTION ( 'NONE',  ( 0.000000000000000000, 0.000000000000000000, 1.000000000000000000 ) ) ;
#6020=DIRECTION ( 'NONE',  ( -1.000000000000000000, -0.000000000000000000, -0.000000000000000000 ) ) ;
#6029=EDGE_CURVE ( 'NONE', #6045, #17299, #5490, .T. ) ;
#6045=VERTEX_POINT ( 'NONE', #5682 ) ;
#6119=FACE_OUTER_BOUND ( 'NONE', #17380, .T. ) ;
#6133=DIRECTION ( 'NONE',  ( 1.000000000000000000, 0.000000000000000000, 0.000000000000000000 ) ) ;
#6193=EDGE_CURVE ( 'NONE', #10924, #6045, #548, .T. ) ;
#6199=AXIS2_PLACEMENT_3D ( 'NONE', #8518, #6895, #3811 ) ;
#6222=ORIENTED_EDGE ( 'NONE', *, *, #13671, .T. ) ;
#6230=DIRECTION ( 'NONE',  ( 1.000000000000000000, 0.000000000000000000, 0.000000000000000000 ) ) ;
#6244=CIRCLE ( 'NONE', #192, 3.323499999999993015 ) ;
#6396=FACE_OUTER_BOUND ( 'NONE', #19047, .T. ) ;
#6466=ADVANCED_FACE ( 'NONE', ( #13464 ), #5151, .T. ) ;
#6474=DIRECTION ( 'NONE',  ( 0.000000000000000000, 0.000000000000000000, 1.000000000000000000 ) ) ;
#6623=DIRECTION ( 'NONE',  ( 1.000000000000000000, 0.000000000000000000, 0.000000000000000000 ) ) ;
#6692=VECTOR ( 'NONE', #10635, 999.9999999999998863 ) ;
#6710=ADVANCED_FACE ( 'NONE', ( #6119 ), #14426, .T. ) ;
#6806=( GEOMETRIC_REPRESENTATION_CONTEXT ( 3 ) GLOBAL_UNCERTAINTY_ASSIGNED_CONTEXT ( ( #3792 ) ) GLOBAL_UNIT_ASSIGNED_CONTEXT ( ( #10030, #1503, #12310 ) ) REPRESENTATION_CONTEXT ( 'NONE', 'WORKASPACE' ) );
#6889=VECTOR ( 'NONE', #12026, 1000.000000000000000 ) ;
#6895=DIRECTION ( 'NONE',  ( -1.000000000000000000, -0.000000000000000000, -0.000000000000000000 ) ) ;
#6943=PLANE ( 'NONE',  #13835 ) ;
#6950=ADVANCED_FACE ( 'NONE', ( #11434 ), #717, .T. ) ;
#6992=CARTESIAN_POINT ( 'NONE',  ( 10.12500000000000178, 0.000000000000000000, 4.000000000000000000 ) ) ;
#7030=VECTOR ( 'NONE', #9111, 999.9999999999998863 ) ;
#7034=DIRECTION ( 'NONE',  ( -1.000000000000000000, 0.000000000000000000, -0.000000000000000000 ) ) ;
#7047=CARTESIAN_POINT ( 'NONE',  ( 112.0000000000000000, 4.484350416777816686E-16, -3.323499999999993015 ) ) ;
#7126=EDGE_LOOP ( 'NONE', ( #335, #1, #14857, #4332 ) ) ;
#7152=DIRECTION ( 'NONE',  ( 0.000000000000000000, 0.000000000000000000, -1.000000000000000000 ) ) ;
#7186=CARTESIAN_POINT ( 'NONE',  ( -1.310841663519413114, 4.898587196589412829E-16, -4.000000000000000000 ) ) ;
#7199=ORIENTED_EDGE ( 'NONE', *, *, #6029, .T. ) ;
#7208=ORIENTED_EDGE ( 'NONE', *, *, #7561, .T. ) ;
#7246=AXIS2_PLACEMENT_3D ( 'NONE', #10537, #5110, #17133 ) ;
#7267=DIRECTION ( 'NONE',  ( 0.000000000000000000, 0.000000000000000000, 1.000000000000000000 ) ) ;
#7270=CARTESIAN_POINT ( 'NONE',  ( 10.12500000000000178, 0.000000000000000000, 0.000000000000000000 ) ) ;
#7295=DIRECTION ( 'NONE',  ( 0.000000000000000000, 0.000000000000000000, 1.000000000000000000 ) ) ;
#7336=ORIENTED_EDGE ( 'NONE', *, *, #16808, .T. ) ;
#7352=CYLINDRICAL_SURFACE ( 'NONE', #16070, 4.000000000000000000 ) ;
#7469=DIRECTION ( 'NONE',  ( -0.7071067811865492381, 0.000000000000000000, 0.7071067811865457964 ) ) ;
#7487=SHAPE_REPRESENTATION_RELATIONSHIP ( 'NONE' , 'NONE' ,  #11438, #8048 ) ;
#7526=CONICAL_SURFACE ( 'NONE', #533, 4.000000000000000000, 0.2132412839022289897 ) ;
#7561=EDGE_CURVE ( 'NONE', #12604, #17114, #10787, .T. ) ;
#7681=VECTOR ( 'NONE', #12209, 999.9999999999998863 ) ;
#7758=AXIS2_PLACEMENT_3D ( 'NONE', #11470, #2259, #14575 ) ;
#7812=LINE ( 'NONE', #15822, #8196 ) ;
#7828=ORIENTED_EDGE ( 'NONE', *, *, #17501, .F. ) ;
#7934=DIRECTION ( 'NONE',  ( 0.000000000000000000, 0.000000000000000000, -1.000000000000000000 ) ) ;
#7979=CIRCLE ( 'NONE', #15979, 4.000000000000000000 ) ;
#7988=CARTESIAN_POINT ( 'NONE',  ( 91.50000000000000000, 0.000000000000000000, 0.000000000000000000 ) ) ;
#7992=LINE ( 'NONE', #12318, #663 ) ;
#8022=ORIENTED_EDGE ( 'NONE', *, *, #5024, .T. ) ;
#8048=ADVANCED_BREP_SHAPE_REPRESENTATION ( '', ( #2965, #16724 ), #16405 ) ;
#8087=CARTESIAN_POINT ( 'NONE',  ( 90.56249999999998579, 0.000000000000000000, 3.796999999999998820 ) ) ;
#8196=VECTOR ( 'NONE', #11021, 999.9999999999998863 ) ;
#8249=( NAMED_UNIT ( * ) SI_UNIT ( $, .STERADIAN. ) SOLID_ANGLE_UNIT ( ) );
#8250=AXIS2_PLACEMENT_3D ( 'NONE', #9445, #18634, #12542 ) ;
#8266=ORIENTED_EDGE ( 'NONE', *, *, #259, .T. ) ;
#8270=ORIENTED_EDGE ( 'NONE', *, *, #15378, .F. ) ;
#8284=AXIS2_PLACEMENT_3D ( 'NONE', #5925, #16643, #12244 ) ;
#8290=DIRECTION ( 'NONE',  ( -1.000000000000000000, -0.000000000000000000, -0.000000000000000000 ) ) ;
#8422=PRESENTATION_STYLE_ASSIGNMENT (( #17522 ) ) ;
#8518=CARTESIAN_POINT ( 'NONE',  ( 111.3234999999999957, 0.000000000000000000, 0.000000000000000000 ) ) ;
#8735=CARTESIAN_POINT ( 'NONE',  ( 91.50000000000000000, 0.000000000000000000, -4.000000000000000000 ) ) ;
#8745=MECHANICAL_DESIGN_GEOMETRIC_PRESENTATION_REPRESENTATION('',(#4264),#6806);
#8791=UNCERTAINTY_MEASURE_WITH_UNIT (LENGTH_MEASURE( 1.000000000000000082E-05 ), #17620, 'distance_accuracy_value', 'NONE');
#8794=DIRECTION ( 'NONE',  ( -1.000000000000000000, -0.000000000000000000, -0.000000000000000000 ) ) ;
#8802=AXIS2_PLACEMENT_3D ( 'NONE', #4172, #19274, #7152 ) ;
#8838=VERTEX_POINT ( 'NONE', #7047 ) ;
#8900=DIRECTION ( 'NONE',  ( -0.9773501006361902110, 2.591706245282799409E-17, -0.2116288751244233268 ) ) ;
#8953=CARTESIAN_POINT ( 'NONE',  ( 0.6764999999999817826, 4.898587196589412829E-16, -4.000000000000000000 ) ) ;
#8954=CARTESIAN_POINT ( 'NONE',  ( 112.0000000000000000, 0.000000000000000000, 0.000000000000000000 ) ) ;
#8958=VERTEX_POINT ( 'NONE', #4072 ) ;
#8967=AXIS2_PLACEMENT_3D ( 'NONE', #7988, #394, #6474 ) ;
#8993=ORIENTED_EDGE ( 'NONE', *, *, #1510, .T. ) ;
#9019=LINE ( 'NONE', #2807, #6889 ) ;
#9057=EDGE_CURVE ( 'NONE', #17114, #1278, #4564, .T. ) ;
#9111=DIRECTION ( 'NONE',  ( 0.9773501006361904331, 2.591706245282795403E-17, 0.2116288751244229938 ) ) ;
#9112=ORIENTED_EDGE ( 'NONE', *, *, #6193, .F. ) ;
#9113=LINE ( 'NONE', #7186, #1522 ) ;
#9151=AXIS2_PLACEMENT_3D ( 'NONE', #17928, #17731, #7295 ) ;
#9204=CARTESIAN_POINT ( 'NONE',  ( 91.50000000000000000, 4.898587196589412829E-16, -4.000000000000000000 ) ) ;
#9230=VERTEX_POINT ( 'NONE', #5729 ) ;
#9366=CARTESIAN_POINT ( 'NONE',  ( 91.50000000000000000, 4.898587196589412829E-16, 4.000000000000000000 ) ) ;
#9430=DIRECTION ( 'NONE',  ( -1.000000000000000000, -0.000000000000000000, -0.000000000000000000 ) ) ;
#9445=CARTESIAN_POINT ( 'NONE',  ( -1.310841663519413114, 0.000000000000000000, 0.000000000000000000 ) ) ;
#9452=CARTESIAN_POINT ( 'NONE',  ( -1.310841663519413114, 0.000000000000000000, 0.000000000000000000 ) ) ;
#9510=ORIENTED_EDGE ( 'NONE', *, *, #667, .F. ) ;
#9517=FACE_OUTER_BOUND ( 'NONE', #2206, .T. ) ;
#9525=AXIS2_PLACEMENT_3D ( 'NONE', #16107, #19186, #3989 ) ;
#9555=DIRECTION ( 'NONE',  ( 1.000000000000000000, 0.000000000000000000, 0.000000000000000000 ) ) ;
#9587=EDGE_LOOP ( 'NONE', ( #14902, #3308, #176, #1963 ) ) ;
#9635=EDGE_LOOP ( 'NONE', ( #2996, #13021, #18011, #13141 ) ) ;
#9712=CIRCLE ( 'NONE', #4271, 3.323500000000020993 ) ;
#9719=CYLINDRICAL_SURFACE ( 'NONE', #8284, 4.000000000000000000 ) ;
#9833=DIRECTION ( 'NONE',  ( 0.000000000000000000, 0.000000000000000000, 1.000000000000000000 ) ) ;
#9863=CARTESIAN_POINT ( 'NONE',  ( 0.000000000000000000, 0.000000000000000000, 0.000000000000000000 ) ) ;
#9869=( LENGTH_UNIT ( ) NAMED_UNIT ( * ) SI_UNIT ( .MILLI., .METRE. ) );
#9927=CIRCLE ( 'NONE', #12153, 4.000000000000000000 ) ;
#9932=CARTESIAN_POINT ( 'NONE',  ( 91.50000000000000000, 0.000000000000000000, 0.000000000000000000 ) ) ;
#9934=CARTESIAN_POINT ( 'NONE',  ( 11.06250000000000000, 4.774285546475956322E-16, -3.797000000000000597 ) ) ;
#9951=EDGE_CURVE ( 'NONE', #12919, #1763, #15188, .T. ) ;
#10030=( LENGTH_UNIT ( ) NAMED_UNIT ( * ) SI_UNIT ( .MILLI., .METRE. ) );
#10047=ORIENTED_EDGE ( 'NONE', *, *, #11034, .F. ) ;
#10063=CARTESIAN_POINT ( 'NONE',  ( 111.3234999999999957, 4.898587196589412829E-16, -4.000000000000000000 ) ) ;
#10110=AXIS2_PLACEMENT_3D ( 'NONE', #13927, #220, #15529 ) ;
#10192=VECTOR ( 'NONE', #15612, 1000.000000000000000 ) ;
#10249=DIRECTION ( 'NONE',  ( 0.000000000000000000, 0.000000000000000000, 1.000000000000000000 ) ) ;
#10300=AXIS2_PLACEMENT_3D ( 'NONE', #17534, #11918, #5903 ) ;
#10321=CARTESIAN_POINT ( 'NONE',  ( 12.00000000000000355, 4.898587196589412829E-16, 4.000000000000000000 ) ) ;
#10377=DIRECTION ( 'NONE',  ( 0.000000000000000000, 0.000000000000000000, -1.000000000000000000 ) ) ;
#10407=EDGE_CURVE ( 'NONE', #8838, #12604, #6244, .T. ) ;
#10417=EDGE_CURVE ( 'NONE', #1763, #12919, #2722, .T. ) ;
#10474=DIRECTION ( 'NONE',  ( 1.000000000000000000, 0.000000000000000000, 0.000000000000000000 ) ) ;
#10510=ORIENTED_EDGE ( 'NONE', *, *, #14366, .F. ) ;
#10537=CARTESIAN_POINT ( 'NONE',  ( -1.310841663519413114, 0.000000000000000000, 0.000000000000000000 ) ) ;
#10540=CARTESIAN_POINT ( 'NONE',  ( 89.62500000000000000, 0.000000000000000000, 0.000000000000000000 ) ) ;
#10553=CIRCLE ( 'NONE', #17264, 4.000000000000000000 ) ;
#10595=ORIENTED_EDGE ( 'NONE', *, *, #9057, .F. ) ;
#10635=DIRECTION ( 'NONE',  ( 0.9773501006361904331, 0.000000000000000000, -0.2116288751244229938 ) ) ;
#10645=CIRCLE ( 'NONE', #5205, 3.323499999999993015 ) ;
#10686=AXIS2_PLACEMENT_3D ( 'NONE', #9863, #6623, #18472 ) ;
#10701=CIRCLE ( 'NONE', #6199, 4.000000000000000000 ) ;
#10702=LINE ( 'NONE', #19399, #18559 ) ;
#10733=ORIENTED_EDGE ( 'NONE', *, *, #731, .T. ) ;
#10736=ORIENTED_EDGE ( 'NONE', *, *, #5772, .T. ) ;
#10755=DIRECTION ( 'NONE',  ( 0.000000000000000000, 0.000000000000000000, 1.000000000000000000 ) ) ;
#10770=ADVANCED_FACE ( 'NONE', ( #6396 ), #13944, .T. ) ;
#10775=FACE_OUTER_BOUND ( 'NONE', #19106, .T. ) ;
#10787=LINE ( 'NONE', #12485, #1352 ) ;
#10909=AXIS2_PLACEMENT_3D ( 'NONE', #12243, #5924, #4338 ) ;
#10912=ADVANCED_FACE ( 'NONE', ( #3810 ), #7526, .T. ) ;
#10924=VERTEX_POINT ( 'NONE', #6992 ) ;
#10938=VECTOR ( 'NONE', #13673, 1000.000000000000000 ) ;
#10983=CONICAL_SURFACE ( 'NONE', #14179, 4.000000000000000000, 0.2132412839022289897 ) ;
#11021=DIRECTION ( 'NONE',  ( -0.9773501006361904331, 2.591706245282795403E-17, -0.2116288751244229938 ) ) ;
#11034=EDGE_CURVE ( 'NONE', #19646, #17299, #18019, .T. ) ;
#11100=ORIENTED_EDGE ( 'NONE', *, *, #15282, .T. ) ;
#11211=ORIENTED_EDGE ( 'NONE', *, *, #774, .F. ) ;
#11361=PRESENTATION_STYLE_ASSIGNMENT (( #3942 ) ) ;
#11394=CARTESIAN_POINT ( 'NONE',  ( 91.50000000000000000, 0.000000000000000000, 4.000000000000000000 ) ) ;
#11423=SURFACE_SIDE_STYLE ('',( #19499 ) ) ;
#11428=ORIENTED_EDGE ( 'NONE', *, *, #13519, .F. ) ;
#11434=FACE_OUTER_BOUND ( 'NONE', #2510, .T. ) ;
#11438=SHAPE_REPRESENTATION ( 'double end studs bm=1.5d_am_AM A M8X100-N', ( #16724 ), #16405 ) ;
#11470=CARTESIAN_POINT ( 'NONE',  ( 91.50000000000000000, 0.000000000000000000, 0.000000000000000000 ) ) ;
#11497=CARTESIAN_POINT ( 'NONE',  ( 112.0000000000000000, 0.000000000000000000, 3.323499999999993015 ) ) ;
#11613=DIRECTION ( 'NONE',  ( 0.000000000000000000, 0.000000000000000000, 1.000000000000000000 ) ) ;
#11654=ADVANCED_FACE ( 'NONE', ( #12776 ), #5346, .T. ) ;
#11658=CARTESIAN_POINT ( 'NONE',  ( 112.0000000000000000, 4.000000000000000000, 0.000000000000000000 ) ) ;
#11663=ORIENTED_EDGE ( 'NONE', *, *, #12335, .T. ) ;
#11818=AXIS2_PLACEMENT_3D ( 'NONE', #2406, #19117, #11613 ) ;
#11848=ORIENTED_EDGE ( 'NONE', *, *, #13671, .F. ) ;
#11851=DIRECTION ( 'NONE',  ( 0.000000000000000000, 0.000000000000000000, -1.000000000000000000 ) ) ;
#11853=CARTESIAN_POINT ( 'NONE',  ( 12.00000000000000355, 0.000000000000000000, 0.000000000000000000 ) ) ;
#11895=ADVANCED_FACE ( 'NONE', ( #18142 ), #4429, .T. ) ;
#11918=DIRECTION ( 'NONE',  ( -1.000000000000000000, -0.000000000000000000, -0.000000000000000000 ) ) ;
#11957=DIRECTION ( 'NONE',  ( 0.000000000000000000, 0.000000000000000000, 1.000000000000000000 ) ) ;
#11978=FACE_OUTER_BOUND ( 'NONE', #9587, .T. ) ;
#11995=CARTESIAN_POINT ( 'NONE',  ( 89.62500000000000000, 0.000000000000000000, 0.000000000000000000 ) ) ;
#12004=CIRCLE ( 'NONE', #3058, 4.000000000000000000 ) ;
#12026=DIRECTION ( 'NONE',  ( -1.000000000000000000, -0.000000000000000000, -0.000000000000000000 ) ) ;
#12037=AXIS2_PLACEMENT_3D ( 'NONE', #7270, #13392, #18100 ) ;
#12038=ORIENTED_EDGE ( 'NONE', *, *, #15449, .F. ) ;
#12045=LINE ( 'NONE', #16849, #10192 ) ;
#12058=FACE_OUTER_BOUND ( 'NONE', #3421, .T. ) ;
#12059=CARTESIAN_POINT ( 'NONE',  ( 11.06250000000000000, 0.000000000000000000, 0.000000000000000000 ) ) ;
#12083=CARTESIAN_POINT ( 'NONE',  ( -1.310841663519413114, 0.000000000000000000, 0.000000000000000000 ) ) ;
#12148=ORIENTED_EDGE ( 'NONE', *, *, #3954, .T. ) ;
#12153=AXIS2_PLACEMENT_3D ( 'NONE', #5718, #16339, #19635 ) ;
#12155=DIRECTION ( 'NONE',  ( -1.000000000000000000, -0.000000000000000000, -0.000000000000000000 ) ) ;
#12209=DIRECTION ( 'NONE',  ( 0.9773501006361904331, 0.000000000000000000, -0.2116288751244229938 ) ) ;
#12243=CARTESIAN_POINT ( 'NONE',  ( 12.00000000000000355, 0.000000000000000000, 0.000000000000000000 ) ) ;
#12244=DIRECTION ( 'NONE',  ( 0.000000000000000000, 0.000000000000000000, 1.000000000000000000 ) ) ;
#12310=( NAMED_UNIT ( * ) SI_UNIT ( $, .STERADIAN. ) SOLID_ANGLE_UNIT ( ) );
#12318=CARTESIAN_POINT ( 'NONE',  ( 0.000000000000000000, 4.070113636966254069E-16, 3.323500000000020993 ) ) ;
#12335=EDGE_CURVE ( 'NONE', #8958, #18746, #9113, .T. ) ;
#12342=CIRCLE ( 'NONE', #9151, 4.000000000000000000 ) ;
#12424=DIRECTION ( 'NONE',  ( -1.000000000000000000, -0.000000000000000000, -0.000000000000000000 ) ) ;
#12485=CARTESIAN_POINT ( 'NONE',  ( 111.3234999999999957, 0.000000000000000000, 4.000000000000000000 ) ) ;
#12533=ADVANCED_FACE ( 'NONE', ( #3790 ), #18776, .T. ) ;
#12542=DIRECTION ( 'NONE',  ( 0.000000000000000000, 0.000000000000000000, 1.000000000000000000 ) ) ;
#12604=VERTEX_POINT ( 'NONE', #11497 ) ;
#12776=FACE_OUTER_BOUND ( 'NONE', #14364, .T. ) ;
#12902=EDGE_LOOP ( 'NONE', ( #17430, #10733 ) ) ;
#12919=VERTEX_POINT ( 'NONE', #13886 ) ;
#12998=CARTESIAN_POINT ( 'NONE',  ( 111.3234999999999957, 0.000000000000000000, 0.000000000000000000 ) ) ;
#13021=ORIENTED_EDGE ( 'NONE', *, *, #15653, .F. ) ;
#13023=DIRECTION ( 'NONE',  ( 1.000000000000000000, 0.000000000000000000, 0.000000000000000000 ) ) ;
#13038=ORIENTED_EDGE ( 'NONE', *, *, #15653, .T. ) ;
#13062=PRODUCT ( 'double end studs bm=1.5d_am_AM A M8X100-N', 'double end studs bm=1.5d_am_AM A M8X100-N', '', ( #5045 ) ) ;
#13141=ORIENTED_EDGE ( 'NONE', *, *, #19516, .T. ) ;
#13206=CARTESIAN_POINT ( 'NONE',  ( -1.310841663519413114, 4.898587196589412829E-16, -4.000000000000000000 ) ) ;
#13218=FILL_AREA_STYLE_COLOUR ( '', #18960 ) ;
#13223=ORIENTED_EDGE ( 'NONE', *, *, #15449, .T. ) ;
#13252=EDGE_CURVE ( 'NONE', #2117, #1278, #18558, .T. ) ;
#13303=DIRECTION ( 'NONE',  ( 0.7071067811865489050, 0.000000000000000000, -0.7071067811865462405 ) ) ;
#13308=DIRECTION ( 'NONE',  ( -1.000000000000000000, -0.000000000000000000, -0.000000000000000000 ) ) ;
#13392=DIRECTION ( 'NONE',  ( -1.000000000000000000, -0.000000000000000000, -0.000000000000000000 ) ) ;
#13401=FILL_AREA_STYLE ('',( #13218 ) ) ;
#13428=CARTESIAN_POINT ( 'NONE',  ( 0.6764999999999817826, 0.000000000000000000, 4.000000000000000000 ) ) ;
#13460=DIRECTION ( 'NONE',  ( 0.000000000000000000, 0.000000000000000000, -1.000000000000000000 ) ) ;
#13464=FACE_OUTER_BOUND ( 'NONE', #2383, .T. ) ;
#13519=EDGE_CURVE ( 'NONE', #8838, #8958, #5725, .T. ) ;
#13671=EDGE_CURVE ( 'NONE', #10924, #15369, #12045, .T. ) ;
#13673=DIRECTION ( 'NONE',  ( -1.000000000000000000, -0.000000000000000000, -0.000000000000000000 ) ) ;
#13677=DIRECTION ( 'NONE',  ( -1.000000000000000000, -0.000000000000000000, -0.000000000000000000 ) ) ;
#13706=CARTESIAN_POINT ( 'NONE',  ( 12.00000000000000355, 0.000000000000000000, -4.000000000000000000 ) ) ;
#13714=ORIENTED_EDGE ( 'NONE', *, *, #15753, .T. ) ;
#13721=ORIENTED_EDGE ( 'NONE', *, *, #13252, .T. ) ;
#13730=LINE ( 'NONE', #8735, #6692 ) ;
#13769=ADVANCED_FACE ( 'NONE', ( #9517 ), #9719, .T. ) ;
#13832=CARTESIAN_POINT ( 'NONE',  ( 91.50000000000000000, 0.000000000000000000, 0.000000000000000000 ) ) ;
#13835=AXIS2_PLACEMENT_3D ( 'NONE', #11658, #7034, #5259 ) ;
#13886=CARTESIAN_POINT ( 'NONE',  ( 11.06250000000000000, 0.000000000000000000, 3.797000000000000597 ) ) ;
#13927=CARTESIAN_POINT ( 'NONE',  ( 0.000000000000000000, 0.000000000000000000, 0.000000000000000000 ) ) ;
#13944=CONICAL_SURFACE ( 'NONE', #10110, 3.323500000000020993, 0.7853981633974463916 ) ;
#14005=AXIS2_PLACEMENT_3D ( 'NONE', #11995, #8794, #7267 ) ;
#14006=FACE_OUTER_BOUND ( 'NONE', #14683, .T. ) ;
#14042=DIRECTION ( 'NONE',  ( 0.000000000000000000, 0.000000000000000000, 1.000000000000000000 ) ) ;
#14063=ADVANCED_FACE ( 'NONE', ( #16958 ), #15752, .F. ) ;
#14083=ORIENTED_EDGE ( 'NONE', *, *, #17501, .T. ) ;
#14162=CIRCLE ( 'NONE', #2022, 4.000000000000000000 ) ;
#14179=AXIS2_PLACEMENT_3D ( 'NONE', #17712, #2587, #5591 ) ;
#14199=ORIENTED_EDGE ( 'NONE', *, *, #5280, .T. ) ;
#14284=EDGE_LOOP ( 'NONE', ( #5466, #14083, #9112, #11211 ) ) ;
#14342=DIRECTION ( 'NONE',  ( -1.000000000000000000, -0.000000000000000000, -0.000000000000000000 ) ) ;
#14360=ORIENTED_EDGE ( 'NONE', *, *, #5537, .F. ) ;
#14364=EDGE_LOOP ( 'NONE', ( #9510, #13038, #15164, #17211 ) ) ;
#14366=EDGE_CURVE ( 'NONE', #2117, #19129, #18136, .T. ) ;
#14426=CONICAL_SURFACE ( 'NONE', #10909, 4.000000000000000000, 0.2132412839022289897 ) ;
#14520=DIRECTION ( 'NONE',  ( -1.000000000000000000, -0.000000000000000000, -0.000000000000000000 ) ) ;
#14575=DIRECTION ( 'NONE',  ( 0.000000000000000000, 0.000000000000000000, 1.000000000000000000 ) ) ;
#14624=DIRECTION ( 'NONE',  ( 0.000000000000000000, 0.000000000000000000, -1.000000000000000000 ) ) ;
#14683=EDGE_LOOP ( 'NONE', ( #8993, #16362, #4701, #10510 ) ) ;
#14729=EDGE_LOOP ( 'NONE', ( #1488, #11663, #12038, #10595 ) ) ;
#14775=CYLINDRICAL_SURFACE ( 'NONE', #15524, 4.000000000000000000 ) ;
#14797=UNCERTAINTY_MEASURE_WITH_UNIT (LENGTH_MEASURE( 1.000000000000000082E-05 ), #9869, 'distance_accuracy_value', 'NONE');
#14811=LINE ( 'NONE', #2305, #449 ) ;
#14857=ORIENTED_EDGE ( 'NONE', *, *, #19583, .F. ) ;
#14902=ORIENTED_EDGE ( 'NONE', *, *, #12335, .F. ) ;
#15048=CONICAL_SURFACE ( 'NONE', #33, 4.000000000000000000, 0.2132412839022289897 ) ;
#15109=CLOSED_SHELL ( 'NONE', ( #900, #4482, #2337, #5231, #15881, #17284, #10770, #11895, #12533, #6950, #14063, #18027, #1380, #6710, #11654, #13769, #19456, #6466, #19248, #10912 ) ) ;
#15156=DIRECTION ( 'NONE',  ( 1.000000000000000000, 0.000000000000000000, 0.000000000000000000 ) ) ;
#15164=ORIENTED_EDGE ( 'NONE', *, *, #14366, .T. ) ;
#15188=CIRCLE ( 'NONE', #8802, 3.797000000000000597 ) ;
#15220=ORIENTED_EDGE ( 'NONE', *, *, #13519, .T. ) ;
#15242=ORIENTED_EDGE ( 'NONE', *, *, #16786, .T. ) ;
#15282=EDGE_CURVE ( 'NONE', #2041, #9230, #9927, .T. ) ;
#15339=ORIENTED_EDGE ( 'NONE', *, *, #10407, .T. ) ;
#15343=ORIENTED_EDGE ( 'NONE', *, *, #259, .F. ) ;
#15369=VERTEX_POINT ( 'NONE', #13428 ) ;
#15378=EDGE_CURVE ( 'NONE', #62, #18746, #13730, .T. ) ;
#15413=CARTESIAN_POINT ( 'NONE',  ( 10.12500000000000178, 0.000000000000000000, 0.000000000000000000 ) ) ;
#15429=CARTESIAN_POINT ( 'NONE',  ( 0.000000000000000000, 0.000000000000000000, 0.000000000000000000 ) ) ;
#15446=ORIENTED_EDGE ( 'NONE', *, *, #16808, .F. ) ;
#15449=EDGE_CURVE ( 'NONE', #1278, #18746, #10553, .T. ) ;
#15524=AXIS2_PLACEMENT_3D ( 'NONE', #17874, #4268, #2655 ) ;
#15529=DIRECTION ( 'NONE',  ( 0.000000000000000000, 0.000000000000000000, -1.000000000000000000 ) ) ;
#15547=VECTOR ( 'NONE', #13303, 1000.000000000000000 ) ;
#15554=DIRECTION ( 'NONE',  ( 1.000000000000000000, 0.000000000000000000, 0.000000000000000000 ) ) ;
#15612=DIRECTION ( 'NONE',  ( -1.000000000000000000, -0.000000000000000000, -0.000000000000000000 ) ) ;
#15653=EDGE_CURVE ( 'NONE', #62, #2117, #965, .T. ) ;
#15752=PLANE ( 'NONE',  #19771 ) ;
#15753=EDGE_CURVE ( 'NONE', #12919, #9230, #4305, .T. ) ;
#15822=CARTESIAN_POINT ( 'NONE',  ( 91.50000000000000000, 4.401380596135586802E-16, -3.593999999999999861 ) ) ;
#15846=CYLINDRICAL_SURFACE ( 'NONE', #17933, 4.000000000000000000 ) ;
#15859=SURFACE_SIDE_STYLE ('',( #2342 ) ) ;
#15881=ADVANCED_FACE ( 'NONE', ( #14006 ), #17275, .T. ) ;
#15902=EDGE_CURVE ( 'NONE', #1763, #2041, #3299, .T. ) ;
#15979=AXIS2_PLACEMENT_3D ( 'NONE', #10540, #6020, #19436 ) ;
#16038=EDGE_LOOP ( 'NONE', ( #2048, #15220, #14360, #17198 ) ) ;
#16043=CARTESIAN_POINT ( 'NONE',  ( 89.62500000000000000, 4.898587196589412829E-16, -4.000000000000000000 ) ) ;
#16070=AXIS2_PLACEMENT_3D ( 'NONE', #12083, #13677, #18185 ) ;
#16101=PRODUCT_DEFINITION_SHAPE ( 'NONE', 'NONE',  #2339 ) ;
#16107=CARTESIAN_POINT ( 'NONE',  ( 12.00000000000000000, 0.000000000000000000, 0.000000000000000000 ) ) ;
#16161=( NAMED_UNIT ( * ) PLANE_ANGLE_UNIT ( ) SI_UNIT ( $, .RADIAN. ) );
#16226=APPLICATION_CONTEXT ( 'automotive_design' ) ;
#16243=DIRECTION ( 'NONE',  ( 0.000000000000000000, 0.000000000000000000, 1.000000000000000000 ) ) ;
#16247=DIRECTION ( 'NONE',  ( -1.000000000000000000, -0.000000000000000000, -0.000000000000000000 ) ) ;
#16276=ORIENTED_EDGE ( 'NONE', *, *, #10417, .T. ) ;
#16292=DIRECTION ( 'NONE',  ( 0.000000000000000000, 0.000000000000000000, 1.000000000000000000 ) ) ;
#16311=FACE_OUTER_BOUND ( 'NONE', #17758, .T. ) ;
#16315=EDGE_CURVE ( 'NONE', #19129, #18274, #7979, .T. ) ;
#16336=DIRECTION ( 'NONE',  ( -1.000000000000000000, -0.000000000000000000, -0.000000000000000000 ) ) ;
#16339=DIRECTION ( 'NONE',  ( -1.000000000000000000, -0.000000000000000000, -0.000000000000000000 ) ) ;
#16362=ORIENTED_EDGE ( 'NONE', *, *, #667, .T. ) ;
#16371=CARTESIAN_POINT ( 'NONE',  ( 0.6764999999999817826, 0.000000000000000000, 0.000000000000000000 ) ) ;
#16388=CIRCLE ( 'NONE', #7758, 4.000000000000000000 ) ;
#16405=( GEOMETRIC_REPRESENTATION_CONTEXT ( 3 ) GLOBAL_UNCERTAINTY_ASSIGNED_CONTEXT ( ( #8791 ) ) GLOBAL_UNIT_ASSIGNED_CONTEXT ( ( #17620, #4010, #19405 ) ) REPRESENTATION_CONTEXT ( 'NONE', 'WORKASPACE' ) );
#16442=CARTESIAN_POINT ( 'NONE',  ( 90.56249999999998579, 0.000000000000000000, 0.000000000000000000 ) ) ;
#16538=CARTESIAN_POINT ( 'NONE',  ( 91.50000000000000000, 0.000000000000000000, 3.593999999999999861 ) ) ;
#16629=AXIS2_PLACEMENT_3D ( 'NONE', #15413, #4904, #17600 ) ;
#16643=DIRECTION ( 'NONE',  ( -1.000000000000000000, -0.000000000000000000, -0.000000000000000000 ) ) ;
#16669=ORIENTED_EDGE ( 'NONE', *, *, #15902, .F. ) ;
#16675=CARTESIAN_POINT ( 'NONE',  ( 0.6764999999999817826, 0.000000000000000000, 0.000000000000000000 ) ) ;
#16724=AXIS2_PLACEMENT_3D ( 'NONE', #17428, #9833, #6230 ) ;
#16786=EDGE_CURVE ( 'NONE', #4617, #15369, #7992, .T. ) ;
#16792=EDGE_LOOP ( 'NONE', ( #4425, #7336, #6222, #12148 ) ) ;
#16808=EDGE_CURVE ( 'NONE', #6045, #10924, #5445, .T. ) ;
#16849=CARTESIAN_POINT ( 'NONE',  ( -1.310841663519413114, 0.000000000000000000, 4.000000000000000000 ) ) ;
#16859=CARTESIAN_POINT ( 'NONE',  ( 112.0000000000000000, 0.000000000000000000, 0.000000000000000000 ) ) ;
#16938=DIRECTION ( 'NONE',  ( -1.000000000000000000, -0.000000000000000000, -0.000000000000000000 ) ) ;
#16958=FACE_OUTER_BOUND ( 'NONE', #12902, .T. ) ;
#17070=EDGE_LOOP ( 'NONE', ( #17271, #7199, #14199, #11848 ) ) ;
#17114=VERTEX_POINT ( 'NONE', #4582 ) ;
#17133=DIRECTION ( 'NONE',  ( 0.000000000000000000, 0.000000000000000000, 1.000000000000000000 ) ) ;
#17198=ORIENTED_EDGE ( 'NONE', *, *, #7561, .F. ) ;
#17199=VECTOR ( 'NONE', #1658, 999.9999999999998863 ) ;
#17211=ORIENTED_EDGE ( 'NONE', *, *, #5024, .F. ) ;
#17253=SHAPE_DEFINITION_REPRESENTATION ( #16101, #11438 ) ;
#17264=AXIS2_PLACEMENT_3D ( 'NONE', #13832, #16938, #3517 ) ;
#17271=ORIENTED_EDGE ( 'NONE', *, *, #6193, .T. ) ;
#17275=CONICAL_SURFACE ( 'NONE', #8967, 3.593999999999999861, 0.2132412839022289897 ) ;
#17284=ADVANCED_FACE ( 'NONE', ( #12058 ), #15048, .T. ) ;
#17299=VERTEX_POINT ( 'NONE', #8953 ) ;
#17310=ORIENTED_EDGE ( 'NONE', *, *, #9951, .T. ) ;
#17355=CIRCLE ( 'NONE', #97, 3.323500000000020993 ) ;
#17380=EDGE_LOOP ( 'NONE', ( #4980, #17310, #3520, #11100 ) ) ;
#17424=LINE ( 'NONE', #217, #1970 ) ;
#17428=CARTESIAN_POINT ( 'NONE',  ( 0.000000000000000000, 0.000000000000000000, 0.000000000000000000 ) ) ;
#17430=ORIENTED_EDGE ( 'NONE', *, *, #285, .T. ) ;
#17501=EDGE_CURVE ( 'NONE', #1763, #6045, #10702, .T. ) ;
#17517=CIRCLE ( 'NONE', #14005, 4.000000000000000000 ) ;
#17519=DIRECTION ( 'NONE',  ( -0.9773501006361902110, 0.000000000000000000, 0.2116288751244233268 ) ) ;
#17522=SURFACE_STYLE_USAGE ( .BOTH. , #11423 ) ;
#17534=CARTESIAN_POINT ( 'NONE',  ( 12.00000000000000000, 0.000000000000000000, 0.000000000000000000 ) ) ;
#17600=DIRECTION ( 'NONE',  ( 0.000000000000000000, 0.000000000000000000, 1.000000000000000000 ) ) ;
#17620=( LENGTH_UNIT ( ) NAMED_UNIT ( * ) SI_UNIT ( .MILLI., .METRE. ) );
#17651=FILL_AREA_STYLE ('',( #18852 ) ) ;
#17669=COLOUR_RGB ( '', 0.40784314, 0.44705882, 0.49803922) ;
#17712=CARTESIAN_POINT ( 'NONE',  ( 91.50000000000000000, 0.000000000000000000, 0.000000000000000000 ) ) ;
#17731=DIRECTION ( 'NONE',  ( -1.000000000000000000, -0.000000000000000000, -0.000000000000000000 ) ) ;
#17758=EDGE_LOOP ( 'NONE', ( #864, #13721, #13223, #8270 ) ) ;
#17816=CIRCLE ( 'NONE', #19407, 4.000000000000000000 ) ;
#17874=CARTESIAN_POINT ( 'NONE',  ( -1.310841663519413114, 0.000000000000000000, 0.000000000000000000 ) ) ;
#17878=CARTESIAN_POINT ( 'NONE',  ( 111.3234999999999957, 0.000000000000000000, 0.000000000000000000 ) ) ;
#17882=CARTESIAN_POINT ( 'NONE',  ( 89.62500000000000000, 0.000000000000000000, 4.000000000000000000 ) ) ;
#17928=CARTESIAN_POINT ( 'NONE',  ( 111.3234999999999957, 0.000000000000000000, 0.000000000000000000 ) ) ;
#17933=AXIS2_PLACEMENT_3D ( 'NONE', #9452, #14342, #14042 ) ;
#17937=DIRECTION ( 'NONE',  ( -0.9773501006361904331, 0.000000000000000000, 0.2116288751244229938 ) ) ;
#18011=ORIENTED_EDGE ( 'NONE', *, *, #15378, .T. ) ;
#18019=LINE ( 'NONE', #2791, #15547 ) ;
#18027=ADVANCED_FACE ( 'NONE', ( #1933 ), #15846, .T. ) ;
#18047=ORIENTED_EDGE ( 'NONE', *, *, #285, .F. ) ;
#18100=DIRECTION ( 'NONE',  ( 0.000000000000000000, 0.000000000000000000, 1.000000000000000000 ) ) ;
#18136=LINE ( 'NONE', #16538, #5910 ) ;
#18142=FACE_OUTER_BOUND ( 'NONE', #17070, .T. ) ;
#18185=DIRECTION ( 'NONE',  ( 0.000000000000000000, 0.000000000000000000, 1.000000000000000000 ) ) ;
#18196=PRODUCT_DEFINITION_CONTEXT ( 'detailed design', #2280, 'design' ) ;
#18273=DIRECTION ( 'NONE',  ( 1.000000000000000000, 0.000000000000000000, 0.000000000000000000 ) ) ;
#18274=VERTEX_POINT ( 'NONE', #16043 ) ;
#18353=DIRECTION ( 'NONE',  ( 0.000000000000000000, 0.000000000000000000, -1.000000000000000000 ) ) ;
#18394=EDGE_CURVE ( 'NONE', #18274, #2041, #17424, .T. ) ;
#18472=DIRECTION ( 'NONE',  ( 0.000000000000000000, 0.000000000000000000, -1.000000000000000000 ) ) ;
#18558=LINE ( 'NONE', #9366, #17199 ) ;
#18559=VECTOR ( 'NONE', #8900, 1000.000000000000227 ) ;
#18634=DIRECTION ( 'NONE',  ( -1.000000000000000000, -0.000000000000000000, -0.000000000000000000 ) ) ;
#18646=DIRECTION ( 'NONE',  ( 0.000000000000000000, 0.000000000000000000, -1.000000000000000000 ) ) ;
#18714=DIRECTION ( 'NONE',  ( 0.000000000000000000, 0.000000000000000000, -1.000000000000000000 ) ) ;
#18746=VERTEX_POINT ( 'NONE', #9204 ) ;
#18776=CONICAL_SURFACE ( 'NONE', #9525, 3.593999999999999861, 0.2132412839022293782 ) ;
#18852=FILL_AREA_STYLE_COLOUR ( '', #17669 ) ;
#18936=MECHANICAL_DESIGN_GEOMETRIC_PRESENTATION_REPRESENTATION('',(#414),#2964);
#18960=COLOUR_RGB ( '', 0.40784314, 0.44705882, 0.49803922) ;
#19047=EDGE_LOOP ( 'NONE', ( #4928, #15242, #19634, #10047 ) ) ;
#19106=EDGE_LOOP ( 'NONE', ( #5641, #18047, #5075, #1691 ) ) ;
#19117=DIRECTION ( 'NONE',  ( -1.000000000000000000, -0.000000000000000000, -0.000000000000000000 ) ) ;
#19129=VERTEX_POINT ( 'NONE', #17882 ) ;
#19186=DIRECTION ( 'NONE',  ( -1.000000000000000000, -0.000000000000000000, -0.000000000000000000 ) ) ;
#19248=ADVANCED_FACE ( 'NONE', ( #11978 ), #7352, .T. ) ;
#19274=DIRECTION ( 'NONE',  ( 1.000000000000000000, 0.000000000000000000, 0.000000000000000000 ) ) ;
#19399=CARTESIAN_POINT ( 'NONE',  ( 12.00000000000000000, 4.401380596135586802E-16, -3.593999999999999861 ) ) ;
#19405=( NAMED_UNIT ( * ) SI_UNIT ( $, .STERADIAN. ) SOLID_ANGLE_UNIT ( ) );
#19407=AXIS2_PLACEMENT_3D ( 'NONE', #16371, #10474, #10377 ) ;
#19436=DIRECTION ( 'NONE',  ( 0.000000000000000000, 0.000000000000000000, 1.000000000000000000 ) ) ;
#19448=CARTESIAN_POINT ( 'NONE',  ( 12.00000000000000355, 0.000000000000000000, 0.000000000000000000 ) ) ;
#19456=ADVANCED_FACE ( 'NONE', ( #3764 ), #6943, .F. ) ;
#19499=SURFACE_STYLE_FILL_AREA ( #13401 ) ;
#19516=EDGE_CURVE ( 'NONE', #18746, #1278, #16388, .T. ) ;
#19549=CARTESIAN_POINT ( 'NONE',  ( 0.000000000000000000, 0.000000000000000000, -3.323500000000020993 ) ) ;
#19583=EDGE_CURVE ( 'NONE', #9230, #2041, #14162, .T. ) ;
#19607=CARTESIAN_POINT ( 'NONE',  ( 12.00000000000000355, 0.000000000000000000, -4.000000000000000000 ) ) ;
#19634=ORIENTED_EDGE ( 'NONE', *, *, #5280, .F. ) ;
#19635=DIRECTION ( 'NONE',  ( 0.000000000000000000, 0.000000000000000000, 1.000000000000000000 ) ) ;
#19646=VERTEX_POINT ( 'NONE', #19549 ) ;
#19649=ORIENTED_EDGE ( 'NONE', *, *, #18394, .F. ) ;
#19744=CARTESIAN_POINT ( 'NONE',  ( 0.000000000000000000, 0.000000000000000000, 0.000000000000000000 ) ) ;
#19771=AXIS2_PLACEMENT_3D ( 'NONE', #3443, #9555, #7934 ) ;
ENDSEC;
END-ISO-10303-21;
